ISO-10303-21;
HEADER;
/* Generated by software containing ST-Developer
 * from STEP Tools, Inc. (www.steptools.com) 
 */

FILE_DESCRIPTION(
/* description */ ('PAT-072'),
/* implementation_level */ '2;1');

FILE_NAME(
/* name */ 'Bonded foot.step',
/* time_stamp */ '2026-10-29T20:11:56-07:00',
/* author */ (''),
/* organization */ (''),
/* preprocessor_version */ 'ST-DEVELOPER v20.2',
/* originating_system */ 'Autodesk Translation Framework v15.17.0.0',
/* authorisation */ '');

FILE_SCHEMA (('AUTOMOTIVE_DESIGN { 1 0 10303 214 3 1 1 }'));
ENDSEC;

DATA;
#10=MECHANICAL_DESIGN_GEOMETRIC_PRESENTATION_REPRESENTATION('',(#361),#11432);
#289=SHAPE_REPRESENTATION_RELATIONSHIP('SRR','None',#11593,#325);
#325=ADVANCED_BREP_SHAPE_REPRESENTATION('',(#397),#11424);
#361=STYLED_ITEM('',(#11833),#397);
#397=MANIFOLD_SOLID_BREP('Body1',#6096);
#737=PLANE('',#7080);
#738=PLANE('',#7081);
#739=PLANE('',#7082);
#740=PLANE('',#7083);
#741=PLANE('',#7084);
#742=PLANE('',#7085);
#1085=FACE_OUTER_BOUND('',#1610,.T.);
#1086=FACE_OUTER_BOUND('',#1611,.T.);
#1087=FACE_OUTER_BOUND('',#1612,.T.);
#1088=FACE_OUTER_BOUND('',#1613,.T.);
#1089=FACE_OUTER_BOUND('',#1614,.T.);
#1090=FACE_OUTER_BOUND('',#1615,.T.);
#1610=EDGE_LOOP('',(#5240,#5241,#5242,#5243));
#1611=EDGE_LOOP('',(#5244,#5245,#5246,#5247));
#1612=EDGE_LOOP('',(#5248,#5249,#5250,#5251));
#1613=EDGE_LOOP('',(#5252,#5253,#5254,#5255));
#1614=EDGE_LOOP('',(#5256,#5257,#5258,#5259));
#1615=EDGE_LOOP('',(#5260,#5261,#5262,#5263));
#2007=LINE('',#10956,#2426);
#2008=LINE('',#10958,#2427);
#2009=LINE('',#10960,#2428);
#2010=LINE('',#10961,#2429);
#2011=LINE('',#10964,#2430);
#2012=LINE('',#10966,#2431);
#2013=LINE('',#10967,#2432);
#2014=LINE('',#10970,#2433);
#2015=LINE('',#10972,#2434);
#2016=LINE('',#10973,#2435);
#2017=LINE('',#10975,#2436);
#2018=LINE('',#10976,#2437);
#2426=VECTOR('',#8716,1.);
#2427=VECTOR('',#8717,1.);
#2428=VECTOR('',#8718,1.);
#2429=VECTOR('',#8719,1.);
#2430=VECTOR('',#8722,1.);
#2431=VECTOR('',#8723,1.);
#2432=VECTOR('',#8724,1.);
#2433=VECTOR('',#8727,1.);
#2434=VECTOR('',#8728,1.);
#2435=VECTOR('',#8729,1.);
#2436=VECTOR('',#8732,1.);
#2437=VECTOR('',#8733,1.);
#3220=VERTEX_POINT('',#10954);
#3221=VERTEX_POINT('',#10955);
#3222=VERTEX_POINT('',#10957);
#3223=VERTEX_POINT('',#10959);
#3224=VERTEX_POINT('',#10963);
#3225=VERTEX_POINT('',#10965);
#3226=VERTEX_POINT('',#10969);
#3227=VERTEX_POINT('',#10971);
#3909=EDGE_CURVE('',#3220,#3221,#2007,.T.);
#3910=EDGE_CURVE('',#3221,#3222,#2008,.T.);
#3911=EDGE_CURVE('',#3223,#3222,#2009,.T.);
#3912=EDGE_CURVE('',#3220,#3223,#2010,.T.);
#3913=EDGE_CURVE('',#3224,#3220,#2011,.T.);
#3914=EDGE_CURVE('',#3225,#3223,#2012,.T.);
#3915=EDGE_CURVE('',#3224,#3225,#2013,.T.);
#3916=EDGE_CURVE('',#3226,#3224,#2014,.T.);
#3917=EDGE_CURVE('',#3227,#3225,#2015,.T.);
#3918=EDGE_CURVE('',#3226,#3227,#2016,.T.);
#3919=EDGE_CURVE('',#3221,#3226,#2017,.T.);
#3920=EDGE_CURVE('',#3222,#3227,#2018,.T.);
#5240=ORIENTED_EDGE('',*,*,#3909,.T.);
#5241=ORIENTED_EDGE('',*,*,#3910,.T.);
#5242=ORIENTED_EDGE('',*,*,#3911,.F.);
#5243=ORIENTED_EDGE('',*,*,#3912,.F.);
#5244=ORIENTED_EDGE('',*,*,#3913,.T.);
#5245=ORIENTED_EDGE('',*,*,#3912,.T.);
#5246=ORIENTED_EDGE('',*,*,#3914,.F.);
#5247=ORIENTED_EDGE('',*,*,#3915,.F.);
#5248=ORIENTED_EDGE('',*,*,#3916,.T.);
#5249=ORIENTED_EDGE('',*,*,#3915,.T.);
#5250=ORIENTED_EDGE('',*,*,#3917,.F.);
#5251=ORIENTED_EDGE('',*,*,#3918,.F.);
#5252=ORIENTED_EDGE('',*,*,#3919,.T.);
#5253=ORIENTED_EDGE('',*,*,#3918,.T.);
#5254=ORIENTED_EDGE('',*,*,#3920,.F.);
#5255=ORIENTED_EDGE('',*,*,#3910,.F.);
#5256=ORIENTED_EDGE('',*,*,#3920,.T.);
#5257=ORIENTED_EDGE('',*,*,#3917,.T.);
#5258=ORIENTED_EDGE('',*,*,#3914,.T.);
#5259=ORIENTED_EDGE('',*,*,#3911,.T.);
#5260=ORIENTED_EDGE('',*,*,#3919,.F.);
#5261=ORIENTED_EDGE('',*,*,#3909,.F.);
#5262=ORIENTED_EDGE('',*,*,#3913,.F.);
#5263=ORIENTED_EDGE('',*,*,#3916,.F.);
#5984=ADVANCED_FACE('',(#1085),#737,.T.);
#5985=ADVANCED_FACE('',(#1086),#738,.T.);
#5986=ADVANCED_FACE('',(#1087),#739,.T.);
#5987=ADVANCED_FACE('',(#1088),#740,.T.);
#5988=ADVANCED_FACE('',(#1089),#741,.T.);
#5989=ADVANCED_FACE('',(#1090),#742,.F.);
#6096=CLOSED_SHELL('',(#5984,#5985,#5986,#5987,#5988,#5989));
#7079=AXIS2_PLACEMENT_3D('',#10952,#8712,#8713);
#7080=AXIS2_PLACEMENT_3D('',#10953,#8714,#8715);
#7081=AXIS2_PLACEMENT_3D('',#10962,#8720,#8721);
#7082=AXIS2_PLACEMENT_3D('',#10968,#8725,#8726);
#7083=AXIS2_PLACEMENT_3D('',#10974,#8730,#8731);
#7084=AXIS2_PLACEMENT_3D('',#10977,#8734,#8735);
#7085=AXIS2_PLACEMENT_3D('',#10978,#8736,#8737);
#8712=DIRECTION('axis',(0.,0.,1.));
#8713=DIRECTION('refdir',(1.,0.,0.));
#8714=DIRECTION('center_axis',(0.,1.,0.));
#8715=DIRECTION('ref_axis',(-1.,0.,0.));
#8716=DIRECTION('',(-1.,0.,0.));
#8717=DIRECTION('',(0.,0.,1.));
#8718=DIRECTION('',(-1.,0.,0.));
#8719=DIRECTION('',(0.,0.,1.));
#8720=DIRECTION('center_axis',(1.,0.,0.));
#8721=DIRECTION('ref_axis',(0.,1.,0.));
#8722=DIRECTION('',(0.,1.,0.));
#8723=DIRECTION('',(0.,1.,0.));
#8724=DIRECTION('',(0.,0.,1.));
#8725=DIRECTION('center_axis',(0.,-1.,0.));
#8726=DIRECTION('ref_axis',(1.,0.,0.));
#8727=DIRECTION('',(1.,0.,0.));
#8728=DIRECTION('',(1.,0.,0.));
#8729=DIRECTION('',(0.,0.,1.));
#8730=DIRECTION('center_axis',(-1.,0.,0.));
#8731=DIRECTION('ref_axis',(0.,-1.,0.));
#8732=DIRECTION('',(0.,-1.,0.));
#8733=DIRECTION('',(0.,-1.,0.));
#8734=DIRECTION('center_axis',(0.,0.,1.));
#8735=DIRECTION('ref_axis',(1.,0.,0.));
#8736=DIRECTION('center_axis',(0.,0.,1.));
#8737=DIRECTION('ref_axis',(1.,0.,0.));
#10952=CARTESIAN_POINT('',(0.,0.,0.));
#10953=CARTESIAN_POINT('Origin',(-5.,3.5,-0.4));
#10954=CARTESIAN_POINT('',(-5.,3.5,-0.4));
#10955=CARTESIAN_POINT('',(-7.,3.5,-0.4));
#10956=CARTESIAN_POINT('',(-5.,3.5,-0.4));
#10957=CARTESIAN_POINT('',(-7.,3.5,0.));
#10958=CARTESIAN_POINT('',(-7.,3.5,-0.4));
#10959=CARTESIAN_POINT('',(-5.,3.5,0.));
#10960=CARTESIAN_POINT('',(-5.,3.5,0.));
#10961=CARTESIAN_POINT('',(-5.,3.5,-0.4));
#10962=CARTESIAN_POINT('Origin',(-5.,-3.5,-0.4));
#10963=CARTESIAN_POINT('',(-5.,-3.5,-0.4));
#10964=CARTESIAN_POINT('',(-5.,-3.5,-0.4));
#10965=CARTESIAN_POINT('',(-5.,-3.5,0.));
#10966=CARTESIAN_POINT('',(-5.,-3.5,0.));
#10967=CARTESIAN_POINT('',(-5.,-3.5,-0.4));
#10968=CARTESIAN_POINT('Origin',(-7.,-3.5,-0.4));
#10969=CARTESIAN_POINT('',(-7.,-3.5,-0.4));
#10970=CARTESIAN_POINT('',(-7.,-3.5,-0.4));
#10971=CARTESIAN_POINT('',(-7.,-3.5,0.));
#10972=CARTESIAN_POINT('',(-7.,-3.5,0.));
#10973=CARTESIAN_POINT('',(-7.,-3.5,-0.4));
#10974=CARTESIAN_POINT('Origin',(-7.,3.5,-0.4));
#10975=CARTESIAN_POINT('',(-7.,3.5,-0.4));
#10976=CARTESIAN_POINT('',(-7.,3.5,0.));
#10977=CARTESIAN_POINT('Origin',(-6.,0.,0.));
#10978=CARTESIAN_POINT('Origin',(-6.,0.,-0.4));
#11385=UNCERTAINTY_MEASURE_WITH_UNIT(LENGTH_MEASURE(0.001),#11433,
'DISTANCE_ACCURACY_VALUE',
'Maximum model space distance between geometric entities at asserted c
onnectivities');
#11393=UNCERTAINTY_MEASURE_WITH_UNIT(LENGTH_MEASURE(0.001),#11433,
'DISTANCE_ACCURACY_VALUE',
'Maximum model space distance between geometric entities at asserted c
onnectivities');
#11424=(
GEOMETRIC_REPRESENTATION_CONTEXT(3)
GLOBAL_UNCERTAINTY_ASSIGNED_CONTEXT((#11385))
GLOBAL_UNIT_ASSIGNED_CONTEXT((#11433,#11435,#11436))
REPRESENTATION_CONTEXT('','3D')
);
#11432=(
GEOMETRIC_REPRESENTATION_CONTEXT(3)
GLOBAL_UNCERTAINTY_ASSIGNED_CONTEXT((#11393))
GLOBAL_UNIT_ASSIGNED_CONTEXT((#11433,#11435,#11436))
REPRESENTATION_CONTEXT('','3D')
);
#11433=(
LENGTH_UNIT()
NAMED_UNIT(*)
SI_UNIT(.CENTI.,.METRE.)
);
#11435=(
NAMED_UNIT(*)
PLANE_ANGLE_UNIT()
SI_UNIT($,.RADIAN.)
);
#11436=(
NAMED_UNIT(*)
SI_UNIT($,.STERADIAN.)
SOLID_ANGLE_UNIT()
);
#11467=SHAPE_DEFINITION_REPRESENTATION(#11505,#11593);
#11505=PRODUCT_DEFINITION_SHAPE('',$,#11632);
#11593=SHAPE_REPRESENTATION('',(#7079),#11424);
#11601=PRODUCT_DEFINITION_CONTEXT('part definition',#11717,'design');
#11632=PRODUCT_DEFINITION('Bonded foot','Bonded foot',#11670,
#11601);
#11670=PRODUCT_DEFINITION_FORMATION('',$,#11749);
#11717=APPLICATION_CONTEXT(
'Core Data for Automotive Mechanical Design Process');
#11718=PRODUCT_CONTEXT('part definition',#11717,'mechanical');
#11749=PRODUCT('Bonded foot','Bonded foot','Bonded foot',
(#11718));
#11827=COLOUR_RGB('Off White',0.89,0.88,0.83);
#11828=FILL_AREA_STYLE_COLOUR('',#11827);
#11829=FILL_AREA_STYLE('',(#11828));
#11830=SURFACE_STYLE_FILL_AREA(#11829);
#11831=SURFACE_SIDE_STYLE('',(#11830));
#11832=SURFACE_STYLE_USAGE(.BOTH.,#11831);
#11833=PRESENTATION_STYLE_ASSIGNMENT((#11832));
ENDSEC;
END-ISO-10303-21;
